ISO-10303-21;
HEADER;
FILE_DESCRIPTION (('STEP AP203'),
    '1' );
FILE_NAME ('1602p_c_12.step',
    '2026-10-31T14:11:27',
    ( '' ),
    ( '' ),
    'SwSTEP 2.0',
    'SolidWorks 2024',
    '' );
FILE_SCHEMA (( 'AUTOMOTIVE_DESIGN' ));
ENDSEC;

DATA;
#35=( LENGTH_UNIT ( ) NAMED_UNIT ( * ) SI_UNIT ( .MILLI., .METRE. ) );
#39=DIRECTION ( 'NONE',  ( -2.982858504577314686E-17, 2.441916418604790135E-15, 1.000000000000000000 ) ) ;
#47=CARTESIAN_POINT ( 'NONE',  ( -19.99995718853209681, 22.95166395734839782, 5.000000000000000000 ) ) ;
#78=DIRECTION ( 'NONE',  ( -0.9997651245102161521, -0.02167246670483388357, 0.000000000000000000 ) ) ;
#105=CIRCLE ( 'NONE', #10016, 1.000000000000000000 ) ;
#114=CARTESIAN_POINT ( 'NONE',  ( -17.00058718854806017, -0.04792152746387602635, 2.500000000000000000 ) ) ;
#167=ORIENTED_EDGE ( 'NONE', *, *, #12338, .T. ) ;
#177=PRODUCT_DEFINITION_SHAPE ( 'NONE', 'NONE',  #10711 ) ;
#196=ORIENTED_EDGE ( 'NONE', *, *, #12338, .F. ) ;
#251=FACE_OUTER_BOUND ( 'NONE', #19236, .T. ) ;
#259=ORIENTED_EDGE ( 'NONE', *, *, #16871, .F. ) ;
#293=LINE ( 'NONE', #15380, #15436 ) ;
#321=CARTESIAN_POINT ( 'NONE',  ( -32.42710143188249816, 10.33427914179039853, 5.000000000000000000 ) ) ;
#342=ORIENTED_EDGE ( 'NONE', *, *, #13446, .T. ) ;
#415=DIRECTION ( 'NONE',  ( 1.000000000000000000, 0.000000000000000000, 0.000000000000000000 ) ) ;
#438=ORIENTED_EDGE ( 'NONE', *, *, #17254, .F. ) ;
#485=ADVANCED_FACE ( 'NONE', ( #13983 ), #21215, .F. ) ;
#589=CIRCLE ( 'NONE', #12378, 2.499999999999999112 ) ;
#643=CARTESIAN_POINT ( 'NONE',  ( -25.44812980900369936, 25.46511081327010118, 2.499999999999940048 ) ) ;
#660=VECTOR ( 'NONE', #10249, 1000.000000000000000 ) ;
#678=PLANE ( 'NONE',  #14136 ) ;
#686=DIRECTION ( 'NONE',  ( 0.9822618273148069346, -0.1875145397033960160, 4.933538860811973842E-16 ) ) ;
#725=DIRECTION ( 'NONE',  ( 0.9822618273148069346, -0.1875145397033960160, 4.845439952583188648E-16 ) ) ;
#862=AXIS2_PLACEMENT_3D ( 'NONE', #21364, #5207, #8777 ) ;
#901=LINE ( 'NONE', #4002, #22309 ) ;
#962=DIRECTION ( 'NONE',  ( -0.9997651245102161521, -0.02167246670483386276, 0.000000000000000000 ) ) ;
#1069=CARTESIAN_POINT ( 'NONE',  ( -29.94686441333699989, 7.343408934390589948, 5.000000000000000000 ) ) ;
#1184=VERTEX_POINT ( 'NONE', #2429 ) ;
#1362=VECTOR ( 'NONE', #19590, 1000.000000000000000 ) ;
#1395=DIRECTION ( 'NONE',  ( -0.02167246311338769799, 0.9997651245880698756, 0.000000000000000000 ) ) ;
#1427=LINE ( 'NONE', #5002, #660 ) ;
#1441=EDGE_CURVE ( 'NONE', #1745, #16463, #9516, .T. ) ;
#1487=EDGE_LOOP ( 'NONE', ( #19660, #19635, #15276, #12559 ) ) ;
#1579=LINE ( 'NONE', #12410, #8740 ) ;
#1599=PRODUCT_DEFINITION_FORMATION_WITH_SPECIFIED_SOURCE ( 'ANY', '', #10100, .NOT_KNOWN. ) ;
#1642=ORIENTED_EDGE ( 'NONE', *, *, #18644, .F. ) ;
#1661=ORIENTED_EDGE ( 'NONE', *, *, #14192, .F. ) ;
#1713=( NAMED_UNIT ( * ) PLANE_ANGLE_UNIT ( ) SI_UNIT ( $, .RADIAN. ) );
#1731=CARTESIAN_POINT ( 'NONE',  ( -19.99975861755289941, 22.95209442650110176, 3.749999999999949818 ) ) ;
#1745=VERTEX_POINT ( 'NONE', #22092 ) ;
#1766=ORIENTED_EDGE ( 'NONE', *, *, #7805, .T. ) ;
#1792=ORIENTED_EDGE ( 'NONE', *, *, #7942, .F. ) ;
#1841=LINE ( 'NONE', #5290, #17933 ) ;
#1888=DIRECTION ( 'NONE',  ( -0.9997651245102160411, -0.02167246670483411256, 0.000000000000000000 ) ) ;
#1940=SHAPE_REPRESENTATION_RELATIONSHIP ( 'NONE' , 'NONE' ,  #9313, #17587 ) ;
#1979=CARTESIAN_POINT ( 'NONE',  ( -25.64161990512560152, 6.365892616704879714, 5.000000000000000000 ) ) ;
#2018=VERTEX_POINT ( 'NONE', #5219 ) ;
#2057=DIRECTION ( 'NONE',  ( -0.9999863470142587030, -0.005225493764090578461, -1.706795877867719251E-17 ) ) ;
#2082=EDGE_CURVE ( 'NONE', #7665, #6041, #6784, .T. ) ;
#2163=ORIENTED_EDGE ( 'NONE', *, *, #3979, .F. ) ;
#2167=EDGE_CURVE ( 'NONE', #3931, #7660, #589, .T. ) ;
#2197=LINE ( 'NONE', #7438, #10653 ) ;
#2218=DIRECTION ( 'NONE',  ( 0.9822618273148069346, -0.1875145397033960160, 4.845439952583188648E-16 ) ) ;
#2253=ORIENTED_EDGE ( 'NONE', *, *, #14709, .T. ) ;
#2271=CARTESIAN_POINT ( 'NONE',  ( -29.01753512594849838, 6.974156885510950588, 2.500000000000000000 ) ) ;
#2319=CARTESIAN_POINT ( 'NONE',  ( -32.65691263631629226, 9.274125246214079965, 5.000000000000000000 ) ) ;
#2320=ORIENTED_EDGE ( 'NONE', *, *, #17834, .T. ) ;
#2376=FACE_BOUND ( 'NONE', #19336, .T. ) ;
#2429=CARTESIAN_POINT ( 'NONE',  ( -13.66074082773489984, 1.277408929928570025, 2.500000000000000000 ) ) ;
#2436=VECTOR ( 'NONE', #22132, 1000.000000000000000 ) ;
#2467=FACE_OUTER_BOUND ( 'NONE', #7732, .T. ) ;
#2476=CARTESIAN_POINT ( 'NONE',  ( -16.50058068176714343, 23.02794805996801841, 2.499999999999950262 ) ) ;
#2497=CARTESIAN_POINT ( 'NONE',  ( -21.66385406723090057, 11.15564796089419985, 2.500000000000000000 ) ) ;
#2569=CARTESIAN_POINT ( 'NONE',  ( 0.000000000000000000, 0.000000000000000000, 0.000000000000000000 ) ) ;
#2786=DIRECTION ( 'NONE',  ( -2.982858504577914959E-17, 2.441916418604795262E-15, 1.000000000000000000 ) ) ;
#2798=PLANE ( 'NONE',  #14426 ) ;
#2820=CYLINDRICAL_SURFACE ( 'NONE', #14450, 2.499999999999999112 ) ;
#2841=ORIENTED_EDGE ( 'NONE', *, *, #3909, .T. ) ;
#2863=EDGE_CURVE ( 'NONE', #6859, #19990, #14271, .T. ) ;
#2919=CARTESIAN_POINT ( 'NONE',  ( -25.49859074735509878, -0.2321374729090470157, 5.000000000000000000 ) ) ;
#2923=CYLINDRICAL_SURFACE ( 'NONE', #14940, 1.000000000000000000 ) ;
#2928=CIRCLE ( 'NONE', #9774, 1.749999999999998668 ) ;
#2929=CYLINDRICAL_SURFACE ( 'NONE', #12042, 1.749999999999998668 ) ;
#2938=ADVANCED_FACE ( 'NONE', ( #10753 ), #17985, .T. ) ;
#2962=ORIENTED_EDGE ( 'NONE', *, *, #5087, .T. ) ;
#2980=ORIENTED_EDGE ( 'NONE', *, *, #2863, .F. ) ;
#3073=DIRECTION ( 'NONE',  ( -0.9997651245880592175, -0.02167246311387461058, 0.000000000000000000 ) ) ;
#3093=LINE ( 'NONE', #6786, #17574 ) ;
#3139=ADVANCED_FACE ( 'NONE', ( #15889 ), #4969, .T. ) ;
#3154=DIRECTION ( 'NONE',  ( 2.982858504577914959E-17, -2.441916418604795262E-15, -1.000000000000000000 ) ) ;
#3162=CARTESIAN_POINT ( 'NONE',  ( -31.64676348097539815, 7.334526001134540785, 3.750000000000000000 ) ) ;
#3211=CARTESIAN_POINT ( 'NONE',  ( -17.00058718854806017, -0.04792152746387602635, 5.000000000000000000 ) ) ;
#3232=DIRECTION ( 'NONE',  ( -0.9997651245102161521, -0.02167246670483386276, 0.000000000000000000 ) ) ;
#3299=EDGE_LOOP ( 'NONE', ( #20641, #18658 ) ) ;
#3357=DIRECTION ( 'NONE',  ( -2.982858504577314686E-17, 2.441916418604790135E-15, 1.000000000000000000 ) ) ;
#3391=ORIENTED_EDGE ( 'NONE', *, *, #9186, .F. ) ;
#3411=EDGE_LOOP ( 'NONE', ( #20484, #342, #9659, #6734 ) ) ;
#3413=DIRECTION ( 'NONE',  ( -0.9997651245880698756, -0.02167246311338769799, 2.310076446361489313E-17 ) ) ;
#3418=CARTESIAN_POINT ( 'NONE',  ( -21.99941281109913760, -0.1562838609880492502, 2.500000000000000000 ) ) ;
#3534=CIRCLE ( 'NONE', #10368, 1.000000000000000000 ) ;
#3561=ADVANCED_FACE ( 'NONE', ( #2467 ), #2820, .F. ) ;
#3601=DIRECTION ( 'NONE',  ( -0.9999863470141812094, -0.005225493778937320352, -1.706795874242040883E-17 ) ) ;
#3668=AXIS2_PLACEMENT_3D ( 'NONE', #17797, #3413, #1395 ) ;
#3690=DIRECTION ( 'NONE',  ( -0.9997651245880592175, -0.02167246311387461752, 0.000000000000000000 ) ) ;
#3728=CARTESIAN_POINT ( 'NONE',  ( -25.49859074735509878, -0.2321374729090530109, 2.500000000000000000 ) ) ;
#3771=AXIS2_PLACEMENT_3D ( 'NONE', #2497, #16611, #13081 ) ;
#3909=EDGE_CURVE ( 'NONE', #8432, #9514, #11865, .T. ) ;
#3931=VERTEX_POINT ( 'NONE', #11831 ) ;
#3945=VERTEX_POINT ( 'NONE', #9700 ) ;
#3979=EDGE_CURVE ( 'NONE', #7239, #8426, #15015, .T. ) ;
#4002=CARTESIAN_POINT ( 'NONE',  ( -25.49859074735509878, -0.2321374729090499855, 3.750000000000000000 ) ) ;
#4012=ORIENTED_EDGE ( 'NONE', *, *, #20853, .F. ) ;
#4042=ORIENTED_EDGE ( 'NONE', *, *, #15951, .T. ) ;
#4095=DIRECTION ( 'NONE',  ( 2.982858504577324546E-17, -2.441916418604795262E-15, -1.000000000000000000 ) ) ;
#4129=ORIENTED_EDGE ( 'NONE', *, *, #2167, .F. ) ;
#4132=ORIENTED_EDGE ( 'NONE', *, *, #21558, .F. ) ;
#4158=DIRECTION ( 'NONE',  ( -0.9997651245102160411, -0.02167246670483410909, 0.000000000000000000 ) ) ;
#4213=CARTESIAN_POINT ( 'NONE',  ( -19.99995718853209681, 22.95166395734829834, 2.499999999999950262 ) ) ;
#4221=CARTESIAN_POINT ( 'NONE',  ( -29.94686441333699989, 7.343408934390589948, 3.750000000000000000 ) ) ;
#4304=VECTOR ( 'NONE', #2057, 1000.000000000000114 ) ;
#4324=FACE_OUTER_BOUND ( 'NONE', #11323, .T. ) ;
#4459=ORIENTED_EDGE ( 'NONE', *, *, #5727, .F. ) ;
#4464=CIRCLE ( 'NONE', #17742, 2.499999999999999112 ) ;
#4533=ORIENTED_EDGE ( 'NONE', *, *, #19898, .T. ) ;
#4603=CARTESIAN_POINT ( 'NONE',  ( -31.64153798721130428, 6.334539654120280083, 2.500000000000000000 ) ) ;
#4642=ADVANCED_FACE ( 'NONE', ( #19157 ), #17370, .F. ) ;
#4715=CARTESIAN_POINT ( 'NONE',  ( -21.99941281109913760, -0.1562838609880462526, 3.750000000000000000 ) ) ;
#4802=VERTEX_POINT ( 'NONE', #114 ) ;
#4917=UNCERTAINTY_MEASURE_WITH_UNIT (LENGTH_MEASURE( 1.000000000000000082E-05 ), #35, 'distance_accuracy_value', 'NONE');
#4969=PLANE ( 'NONE',  #3668 ) ;
#5002=CARTESIAN_POINT ( 'NONE',  ( -29.94163891957289891, 6.343422587376370103, 3.750000000000000000 ) ) ;
#5005=ORIENTED_EDGE ( 'NONE', *, *, #9084, .T. ) ;
#5019=CARTESIAN_POINT ( 'NONE',  ( -19.99975861755289941, 22.95209442650110176, 5.000000000000000000 ) ) ;
#5054=ORIENTED_EDGE ( 'NONE', *, *, #18407, .F. ) ;
#5069=ADVANCED_FACE ( 'NONE', ( #2376, #5691, #12947 ), #9647, .F. ) ;
#5087=EDGE_CURVE ( 'NONE', #7660, #3931, #8725, .T. ) ;
#5207=DIRECTION ( 'NONE',  ( -2.982858504577330093E-17, 2.441916418604790135E-15, 1.000000000000000000 ) ) ;
#5219=CARTESIAN_POINT ( 'NONE',  ( -13.66074082773489984, 1.277408929928580017, 5.000000000000000000 ) ) ;
#5290=CARTESIAN_POINT ( 'NONE',  ( -32.65691263631629226, 9.274125246214069307, 2.500000000000000000 ) ) ;
#5353=ORIENTED_EDGE ( 'NONE', *, *, #19159, .F. ) ;
#5432=AXIS2_PLACEMENT_3D ( 'NONE', #5019, #19620, #3232 ) ;
#5454=EDGE_CURVE ( 'NONE', #18495, #20452, #2197, .T. ) ;
#5481=CARTESIAN_POINT ( 'NONE',  ( -19.49999999982519938, -0.1021026942257659970, 5.000000000000000000 ) ) ;
#5533=ADVANCED_FACE ( 'NONE', ( #9933 ), #2798, .T. ) ;
#5534=ORIENTED_EDGE ( 'NONE', *, *, #3979, .T. ) ;
#5573=ORIENTED_EDGE ( 'NONE', *, *, #17834, .F. ) ;
#5586=ORIENTED_EDGE ( 'NONE', *, *, #22048, .T. ) ;
#5642=DIRECTION ( 'NONE',  ( -2.982858504577319616E-17, 2.441916418604790135E-15, 1.000000000000000000 ) ) ;
#5669=ORIENTED_EDGE ( 'NONE', *, *, #18407, .T. ) ;
#5691=FACE_BOUND ( 'NONE', #3299, .T. ) ;
#5727=EDGE_CURVE ( 'NONE', #3945, #8426, #1579, .T. ) ;
#5729=ORIENTED_EDGE ( 'NONE', *, *, #17143, .F. ) ;
#5830=VERTEX_POINT ( 'NONE', #7635 ) ;
#5876=CARTESIAN_POINT ( 'NONE',  ( -32.42710143188249816, 10.33427914179039853, 3.750000000000000000 ) ) ;
#5972=APPLICATION_CONTEXT ( 'configuration controlled 3d designs of mechanical parts and assemblies' ) ;
#5975=LINE ( 'NONE', #20463, #11911 ) ;
#5987=LINE ( 'NONE', #8013, #2436 ) ;
#6041=VERTEX_POINT ( 'NONE', #13111 ) ;
#6043=ADVANCED_FACE ( 'NONE', ( #4324 ), #14993, .F. ) ;
#6053=AXIS2_PLACEMENT_3D ( 'NONE', #19042, #16892, #11590 ) ;
#6055=ORIENTED_EDGE ( 'NONE', *, *, #11608, .F. ) ;
#6060=ORIENTED_EDGE ( 'NONE', *, *, #14192, .T. ) ;
#6081=EDGE_CURVE ( 'NONE', #1184, #18635, #17035, .T. ) ;
#6161=DIRECTION ( 'NONE',  ( -2.982858504577240114E-17, 2.441916418604790135E-15, 1.000000000000000000 ) ) ;
#6175=CARTESIAN_POINT ( 'NONE',  ( -31.64676348097539815, 7.334526001134540785, 2.500000000000000000 ) ) ;
#6198=VECTOR ( 'NONE', #7320, 1000.000000000000000 ) ;
#6329=DIRECTION ( 'NONE',  ( -0.4188360644630711449, -0.9080618652410672453, 2.204917890671980836E-15 ) ) ;
#6380=CARTESIAN_POINT ( 'NONE',  ( -19.49999999982519938, -0.1021026942257689946, 3.750000000000000000 ) ) ;
#6432=DIRECTION ( 'NONE',  ( -2.982858504577314686E-17, 2.441916418604790135E-15, 1.000000000000000000 ) ) ;
#6445=EDGE_CURVE ( 'NONE', #2018, #7239, #8117, .T. ) ;
#6535=MECHANICAL_CONTEXT ( 'NONE', #7911, 'mechanical' ) ;
#6536=AXIS2_PLACEMENT_3D ( 'NONE', #9299, #7409, #19986 ) ;
#6548=CARTESIAN_POINT ( 'NONE',  ( -29.94163891957289891, 6.343422587376370103, 2.500000000000000000 ) ) ;
#6655=DIRECTION ( 'NONE',  ( -2.982858504577314686E-17, 2.441916418604790135E-15, 1.000000000000000000 ) ) ;
#6734=ORIENTED_EDGE ( 'NONE', *, *, #7042, .T. ) ;
#6784=LINE ( 'NONE', #14010, #1362 ) ;
#6786=CARTESIAN_POINT ( 'NONE',  ( -16.50058068176714343, 23.02794805996801841, 3.749999999999949818 ) ) ;
#6838=DIRECTION ( 'NONE',  ( -0.9080618652418041004, 0.4188360644614733674, -1.040834085574019418E-15 ) ) ;
#6859=VERTEX_POINT ( 'NONE', #19588 ) ;
#6954=AXIS2_PLACEMENT_3D ( 'NONE', #22182, #22066, #18414 ) ;
#6965=ORIENTED_EDGE ( 'NONE', *, *, #11027, .F. ) ;
#7042=EDGE_CURVE ( 'NONE', #1184, #2018, #7368, .T. ) ;
#7060=DIRECTION ( 'NONE',  ( -0.9997651245102161521, -0.02167246670483386276, 0.000000000000000000 ) ) ;
#7069=ADVANCED_FACE ( 'NONE', ( #15169 ), #678, .T. ) ;
#7101=ORIENTED_EDGE ( 'NONE', *, *, #5727, .T. ) ;
#7225=DIRECTION ( 'NONE',  ( -0.005225493778937319485, 0.9999863470141810984, -2.442038948240150648E-15 ) ) ;
#7239=VERTEX_POINT ( 'NONE', #2919 ) ;
#7244=DIRECTION ( 'NONE',  ( 2.982858504577314686E-17, -2.441916418604790135E-15, -1.000000000000000000 ) ) ;
#7297=ORIENTED_EDGE ( 'NONE', *, *, #19898, .F. ) ;
#7320=DIRECTION ( 'NONE',  ( 0.4188360644630711449, 0.9080618652410672453, -2.204917890671980836E-15 ) ) ;
#7322=DIRECTION ( 'NONE',  ( 0.9822591002358885826, -0.1875288244611549582, 4.336808689942019215E-16 ) ) ;
#7334=VERTEX_POINT ( 'NONE', #3728 ) ;
#7368=LINE ( 'NONE', #7704, #20581 ) ;
#7409=DIRECTION ( 'NONE',  ( -2.982858504577894622E-17, 2.441916418604795262E-15, 1.000000000000000000 ) ) ;
#7415=LINE ( 'NONE', #21642, #4304 ) ;
#7438=CARTESIAN_POINT ( 'NONE',  ( -32.65691263631629226, 9.274125246214079965, 3.750000000000000000 ) ) ;
#7450=CARTESIAN_POINT ( 'NONE',  ( -25.44812980900369936, 25.46511081327010118, 4.999999999999940492 ) ) ;
#7533=VERTEX_POINT ( 'NONE', #6548 ) ;
#7635=CARTESIAN_POINT ( 'NONE',  ( -32.64674982798959491, 7.329300507370480666, 5.000000000000000000 ) ) ;
#7660=VERTEX_POINT ( 'NONE', #3211 ) ;
#7665=VERTEX_POINT ( 'NONE', #14013 ) ;
#7704=CARTESIAN_POINT ( 'NONE',  ( -13.66074082773489984, 1.277408929928570025, 3.750000000000000000 ) ) ;
#7732=EDGE_LOOP ( 'NONE', ( #5054, #10935, #9902, #9327 ) ) ;
#7781=DIRECTION ( 'NONE',  ( 0.9822591002358885826, -0.1875288244611549582, 5.059610138265688673E-16 ) ) ;
#7786=DIRECTION ( 'NONE',  ( 1.000000000000000000, 2.982858504577319616E-17, 8.758115402030109610E-48 ) ) ;
#7805=EDGE_CURVE ( 'NONE', #19990, #16463, #3093, .T. ) ;
#7814=CARTESIAN_POINT ( 'NONE',  ( -17.00058718854806017, -0.04792152746387605411, 3.750000000000000000 ) ) ;
#7872=ORIENTED_EDGE ( 'NONE', *, *, #7042, .F. ) ;
#7911=APPLICATION_CONTEXT ( 'configuration controlled 3d designs of mechanical parts and assemblies' ) ;
#7942=EDGE_CURVE ( 'NONE', #6041, #5830, #22095, .T. ) ;
#8004=CARTESIAN_POINT ( 'NONE',  ( -19.99975861755289941, 22.95209442650110176, 5.000000000000000000 ) ) ;
#8013=CARTESIAN_POINT ( 'NONE',  ( -23.49893655333865894, 22.87624079303418156, 3.749999999999949818 ) ) ;
#8024=DIRECTION ( 'NONE',  ( 0.005225493764090578461, -0.9999863470142587030, 2.442038948239898212E-15 ) ) ;
#8117=CIRCLE ( 'NONE', #11168, 6.000000000001507239 ) ;
#8143=CARTESIAN_POINT ( 'NONE',  ( 34.24699604337060066, 12.59578995394270073, 3.750000000000000000 ) ) ;
#8181=EDGE_CURVE ( 'NONE', #9514, #2018, #12286, .T. ) ;
#8192=DIRECTION ( 'NONE',  ( -2.982858504577324546E-17, 2.441916418604795262E-15, 1.000000000000000000 ) ) ;
#8329=AXIS2_PLACEMENT_3D ( 'NONE', #22472, #18575, #725 ) ;
#8348=DIRECTION ( 'NONE',  ( -0.9997651245102161521, -0.02167246670483386276, 0.000000000000000000 ) ) ;
#8426=VERTEX_POINT ( 'NONE', #1979 ) ;
#8432=VERTEX_POINT ( 'NONE', #7450 ) ;
#8442=AXIS2_PLACEMENT_3D ( 'NONE', #6380, #17197, #18972 ) ;
#8514=VECTOR ( 'NONE', #13123, 1000.000000000000000 ) ;
#8529=CARTESIAN_POINT ( 'NONE',  ( -27.39120887301850260, 6.327965799971420502, 3.750000000000000000 ) ) ;
#8555=CARTESIAN_POINT ( 'NONE',  ( -19.49999999982360066, -0.1021026942259639914, 2.500000000000000000 ) ) ;
#8557=ORIENTED_EDGE ( 'NONE', *, *, #1441, .F. ) ;
#8625=DIRECTION ( 'NONE',  ( -0.9999863470142589250, -0.005225493764064552404, 0.000000000000000000 ) ) ;
#8725=CIRCLE ( 'NONE', #20081, 2.499999999999999112 ) ;
#8740=VECTOR ( 'NONE', #17753, 1000.000000000000000 ) ;
#8751=EDGE_LOOP ( 'NONE', ( #13244, #19335, #2320, #21920 ) ) ;
#8766=EDGE_LOOP ( 'NONE', ( #9576, #19312, #13989, #5586 ) ) ;
#8777=DIRECTION ( 'NONE',  ( 0.9822591002358885826, -0.1875288244611549582, 5.059610138265688673E-16 ) ) ;
#8862=ADVANCED_FACE ( 'NONE', ( #17766 ), #2923, .T. ) ;
#8906=ORIENTED_EDGE ( 'NONE', *, *, #2167, .T. ) ;
#8998=CIRCLE ( 'NONE', #21871, 2.500000000028978597 ) ;
#9084=EDGE_CURVE ( 'NONE', #6859, #1745, #5987, .T. ) ;
#9096=DIRECTION ( 'NONE',  ( 0.005225493778937319485, -0.9999863470141810984, 2.442038948240150648E-15 ) ) ;
#9158=ORIENTED_EDGE ( 'NONE', *, *, #13259, .F. ) ;
#9176=AXIS2_PLACEMENT_3D ( 'NONE', #8143, #13155, #2218 ) ;
#9186=EDGE_CURVE ( 'NONE', #10599, #23068, #9918, .T. ) ;
#9299=CARTESIAN_POINT ( 'NONE',  ( -30.15694676875160241, 9.287188980624568657, 3.750000000000000000 ) ) ;
#9313=SHAPE_REPRESENTATION ( '1602p_c_12', ( #12739 ), #14249 ) ;
#9327=ORIENTED_EDGE ( 'NONE', *, *, #5087, .F. ) ;
#9365=DIRECTION ( 'NONE',  ( -2.982858504577319616E-17, 2.441916418604790135E-15, 1.000000000000000000 ) ) ;
#9472=CARTESIAN_POINT ( 'NONE',  ( -14.10640258711669937, 21.82649101058139962, 3.749999999999949818 ) ) ;
#9484=DIRECTION ( 'NONE',  ( -0.9080618652410672453, 0.4188360644630710894, -1.049848863090360721E-15 ) ) ;
#9514=VERTEX_POINT ( 'NONE', #21411 ) ;
#9516=CIRCLE ( 'NONE', #10664, 3.500000000000000444 ) ;
#9550=DIRECTION ( 'NONE',  ( -2.982858504577314686E-17, 2.441916418604790135E-15, 1.000000000000000000 ) ) ;
#9576=ORIENTED_EDGE ( 'NONE', *, *, #13259, .T. ) ;
#9578=CARTESIAN_POINT ( 'NONE',  ( -29.94163891957289891, 6.343422587376370103, 3.750000000000000000 ) ) ;
#9579=VERTEX_POINT ( 'NONE', #2271 ) ;
#9647=PLANE ( 'NONE',  #3771 ) ;
#9659=ORIENTED_EDGE ( 'NONE', *, *, #11862, .T. ) ;
#9699=DIRECTION ( 'NONE',  ( 0.005225493764075828107, -0.9999863470142589250, 2.602085213965210642E-15 ) ) ;
#9700=CARTESIAN_POINT ( 'NONE',  ( -25.64161990512560152, 6.365892616704869944, 2.500000000000000000 ) ) ;
#9774=AXIS2_PLACEMENT_3D ( 'NONE', #19984, #14752, #21764 ) ;
#9902=ORIENTED_EDGE ( 'NONE', *, *, #21893, .T. ) ;
#9918=LINE ( 'NONE', #5876, #8514 ) ;
#9933=FACE_OUTER_BOUND ( 'NONE', #20277, .T. ) ;
#10016=AXIS2_PLACEMENT_3D ( 'NONE', #1069, #4095, #9699 ) ;
#10054=CARTESIAN_POINT ( 'NONE',  ( -32.42710143188249816, 10.33427914179039853, 2.500000000000000000 ) ) ;
#10081=CYLINDRICAL_SURFACE ( 'NONE', #8442, 6.000000000001507239 ) ;
#10100=PRODUCT ( '1602p_c_12', '1602p_c_12', '', ( #6535 ) ) ;
#10140=EDGE_LOOP ( 'NONE', ( #196, #1766, #8557, #11290 ) ) ;
#10158=CIRCLE ( 'NONE', #17351, 2.500000000028978597 ) ;
#10249=DIRECTION ( 'NONE',  ( -2.982858504577319616E-17, 2.441916418604790135E-15, 1.000000000000000000 ) ) ;
#10361=AXIS2_PLACEMENT_3D ( 'NONE', #23153, #6432, #962 ) ;
#10368=AXIS2_PLACEMENT_3D ( 'NONE', #11901, #8192, #17092 ) ;
#10532=VECTOR ( 'NONE', #20982, 1000.000000000000000 ) ;
#10558=DIRECTION ( 'NONE',  ( -2.982858504577314686E-17, 2.441916418604790135E-15, 1.000000000000000000 ) ) ;
#10599=VERTEX_POINT ( 'NONE', #10054 ) ;
#10653=VECTOR ( 'NONE', #5642, 1000.000000000000000 ) ;
#10658=CARTESIAN_POINT ( 'NONE',  ( -25.44812980900369936, 25.46511081327010118, 4.999999999999940492 ) ) ;
#10664=AXIS2_PLACEMENT_3D ( 'NONE', #8004, #15238, #8348 ) ;
#10711=PRODUCT_DEFINITION ( 'UNKNOWN', '', #1599, #13735 ) ;
#10745=AXIS2_PLACEMENT_3D ( 'NONE', #15373, #11491, #7786 ) ;
#10753=FACE_OUTER_BOUND ( 'NONE', #8766, .T. ) ;
#10870=DIRECTION ( 'NONE',  ( -0.005225493778937319485, 0.9999863470141810984, 0.000000000000000000 ) ) ;
#10935=ORIENTED_EDGE ( 'NONE', *, *, #15033, .F. ) ;
#10942=CIRCLE ( 'NONE', #16225, 3.500000000000000444 ) ;
#10982=DIRECTION ( 'NONE',  ( -2.982858504577319616E-17, 2.441916418604790135E-15, 1.000000000000000000 ) ) ;
#11027=EDGE_CURVE ( 'NONE', #9579, #3945, #2928, .T. ) ;
#11091=VECTOR ( 'NONE', #22165, 1000.000000000000000 ) ;
#11157=CIRCLE ( 'NONE', #13797, 5.999999999999998224 ) ;
#11168=AXIS2_PLACEMENT_3D ( 'NONE', #5481, #14625, #3690 ) ;
#11271=EDGE_CURVE ( 'NONE', #7533, #21418, #1427, .T. ) ;
#11275=DIRECTION ( 'NONE',  ( -2.982858504577314686E-17, 2.441916418604790135E-15, 1.000000000000000000 ) ) ;
#11276=FACE_OUTER_BOUND ( 'NONE', #14754, .T. ) ;
#11290=ORIENTED_EDGE ( 'NONE', *, *, #9084, .F. ) ;
#11323=EDGE_LOOP ( 'NONE', ( #259, #5669, #4129, #11794 ) ) ;
#11462=ORIENTED_EDGE ( 'NONE', *, *, #13446, .F. ) ;
#11491=DIRECTION ( 'NONE',  ( -7.283891156702289181E-32, 2.441916418604790135E-15, 1.000000000000000000 ) ) ;
#11496=DIRECTION ( 'NONE',  ( -2.982858504577324546E-17, 2.441916418604800390E-15, 1.000000000000000000 ) ) ;
#11588=ORIENTED_EDGE ( 'NONE', *, *, #2863, .T. ) ;
#11590=DIRECTION ( 'NONE',  ( -0.9997651245102160411, -0.02167246670483410909, 0.000000000000000000 ) ) ;
#11608=EDGE_CURVE ( 'NONE', #9579, #22503, #14960, .T. ) ;
#11633=ORIENTED_EDGE ( 'NONE', *, *, #6081, .F. ) ;
#11746=DIRECTION ( 'NONE',  ( -2.982858504577314686E-17, 2.441916418604790135E-15, 1.000000000000000000 ) ) ;
#11794=ORIENTED_EDGE ( 'NONE', *, *, #21893, .F. ) ;
#11831=CARTESIAN_POINT ( 'NONE',  ( -21.99941281109913760, -0.1562838609880432272, 5.000000000000000000 ) ) ;
#11860=VECTOR ( 'NONE', #10982, 1000.000000000000000 ) ;
#11862=EDGE_CURVE ( 'NONE', #7334, #1184, #17765, .T. ) ;
#11865=CIRCLE ( 'NONE', #15585, 5.999999999999998224 ) ;
#11901=CARTESIAN_POINT ( 'NONE',  ( -29.94686441333699989, 7.343408934390579290, 2.500000000000000000 ) ) ;
#11911=VECTOR ( 'NONE', #6329, 1000.000000000000000 ) ;
#11932=DIRECTION ( 'NONE',  ( -2.982858504577324546E-17, 2.441916418604790135E-15, 1.000000000000000000 ) ) ;
#12012=ORIENTED_EDGE ( 'NONE', *, *, #17143, .T. ) ;
#12031=CARTESIAN_POINT ( 'NONE',  ( -25.64161990512560152, 6.365892616704869944, 2.500000000000000000 ) ) ;
#12042=AXIS2_PLACEMENT_3D ( 'NONE', #8529, #23092, #14210 ) ;
#12195=CARTESIAN_POINT ( 'NONE',  ( -30.15694676875160241, 9.287188980624568657, 5.000000000000000000 ) ) ;
#12286=CIRCLE ( 'NONE', #22147, 49.22658835543909817 ) ;
#12338=EDGE_CURVE ( 'NONE', #19990, #6859, #10942, .T. ) ;
#12378=AXIS2_PLACEMENT_3D ( 'NONE', #18285, #7244, #14824 ) ;
#12410=CARTESIAN_POINT ( 'NONE',  ( -25.64161990512560152, 6.365892616704879714, 3.750000000000000000 ) ) ;
#12476=SHAPE_DEFINITION_REPRESENTATION ( #177, #9313 ) ;
#12484=CLOSED_SHELL ( 'NONE', ( #6043, #4642, #485, #3561, #5069, #3139, #21835, #20457, #5533, #8862, #2938, #16016, #7069, #16911, #15741, #18264, #18827 ) ) ;
#12559=ORIENTED_EDGE ( 'NONE', *, *, #11608, .T. ) ;
#12582=CYLINDRICAL_SURFACE ( 'NONE', #862, 5.999999999999998224 ) ;
#12657=CIRCLE ( 'NONE', #5432, 3.500000000000000444 ) ;
#12663=DIRECTION ( 'NONE',  ( -0.9997651245102161521, -0.02167246670483386276, 0.000000000000000000 ) ) ;
#12691=CARTESIAN_POINT ( 'NONE',  ( -32.65691263631629226, 9.274125246214079965, 5.000000000000000000 ) ) ;
#12739=AXIS2_PLACEMENT_3D ( 'NONE', #2569, #13380, #415 ) ;
#12947=FACE_OUTER_BOUND ( 'NONE', #16827, .T. ) ;
#13081=DIRECTION ( 'NONE',  ( 1.000000000000000000, 2.982858504577319616E-17, 8.758115402030109610E-48 ) ) ;
#13111=CARTESIAN_POINT ( 'NONE',  ( -31.64153798721130428, 6.334539654120280083, 5.000000000000000000 ) ) ;
#13123=DIRECTION ( 'NONE',  ( -2.982858504577319616E-17, 2.441916418604790135E-15, 1.000000000000000000 ) ) ;
#13155=DIRECTION ( 'NONE',  ( -2.982858504577249974E-17, 2.441916418604790135E-15, 1.000000000000000000 ) ) ;
#13244=ORIENTED_EDGE ( 'NONE', *, *, #7942, .T. ) ;
#13245=FACE_BOUND ( 'NONE', #21521, .T. ) ;
#13249=FACE_OUTER_BOUND ( 'NONE', #1487, .T. ) ;
#13258=ORIENTED_EDGE ( 'NONE', *, *, #11027, .T. ) ;
#13259=EDGE_CURVE ( 'NONE', #5830, #20452, #18148, .T. ) ;
#13380=DIRECTION ( 'NONE',  ( 0.000000000000000000, 0.000000000000000000, 1.000000000000000000 ) ) ;
#13428=DIRECTION ( 'NONE',  ( -2.982858504577319616E-17, 2.441916418604790135E-15, 1.000000000000000000 ) ) ;
#13436=ORIENTED_EDGE ( 'NONE', *, *, #9186, .T. ) ;
#13446=EDGE_CURVE ( 'NONE', #7239, #7334, #901, .T. ) ;
#13525=ORIENTED_EDGE ( 'NONE', *, *, #20853, .T. ) ;
#13529=CARTESIAN_POINT ( 'NONE',  ( -19.49999999982519938, -0.1021026942257719922, 2.500000000000000000 ) ) ;
#13596=FACE_OUTER_BOUND ( 'NONE', #19183, .T. ) ;
#13653=ORIENTED_EDGE ( 'NONE', *, *, #8181, .T. ) ;
#13735=DESIGN_CONTEXT ( 'detailed design', #5972, 'design' ) ;
#13797=AXIS2_PLACEMENT_3D ( 'NONE', #4213, #11932, #7781 ) ;
#13800=VECTOR ( 'NONE', #15050, 1000.000000000000000 ) ;
#13837=ORIENTED_EDGE ( 'NONE', *, *, #19159, .T. ) ;
#13983=FACE_OUTER_BOUND ( 'NONE', #14729, .T. ) ;
#13989=ORIENTED_EDGE ( 'NONE', *, *, #18644, .T. ) ;
#14010=CARTESIAN_POINT ( 'NONE',  ( -31.64153798721130428, 6.334539654120280083, 3.750000000000000000 ) ) ;
#14013=CARTESIAN_POINT ( 'NONE',  ( -31.64153798721130428, 6.334539654120280083, 2.500000000000000000 ) ) ;
#14093=ORIENTED_EDGE ( 'NONE', *, *, #8181, .F. ) ;
#14136=AXIS2_PLACEMENT_3D ( 'NONE', #22175, #9484, #18770 ) ;
#14192=EDGE_CURVE ( 'NONE', #10599, #18495, #8998, .T. ) ;
#14210=DIRECTION ( 'NONE',  ( -0.9997651245102161521, -0.02167246670483388357, 0.000000000000000000 ) ) ;
#14249=( GEOMETRIC_REPRESENTATION_CONTEXT ( 3 ) GLOBAL_UNCERTAINTY_ASSIGNED_CONTEXT ( ( #4917 ) ) GLOBAL_UNIT_ASSIGNED_CONTEXT ( ( #35, #1713, #23435 ) ) REPRESENTATION_CONTEXT ( 'NONE', 'WORKASPACE' ) );
#14269=CIRCLE ( 'NONE', #18456, 1.749999999999998668 ) ;
#14271=CIRCLE ( 'NONE', #16545, 3.500000000000000444 ) ;
#14397=CARTESIAN_POINT ( 'NONE',  ( -19.99975861755289941, 22.95209442650110176, 2.499999999999950262 ) ) ;
#14426=AXIS2_PLACEMENT_3D ( 'NONE', #9578, #8024, #16809 ) ;
#14450=AXIS2_PLACEMENT_3D ( 'NONE', #20740, #11746, #18624 ) ;
#14566=ORIENTED_EDGE ( 'NONE', *, *, #2082, .F. ) ;
#14618=ORIENTED_EDGE ( 'NONE', *, *, #7805, .F. ) ;
#14625=DIRECTION ( 'NONE',  ( 2.982858504577314686E-17, -2.441916418604790135E-15, -1.000000000000000000 ) ) ;
#14709=EDGE_CURVE ( 'NONE', #3945, #7334, #17604, .T. ) ;
#14729=EDGE_LOOP ( 'NONE', ( #14618, #2980, #5005, #18280 ) ) ;
#14752=DIRECTION ( 'NONE',  ( 2.982858504577314686E-17, -2.441916418604790135E-15, -1.000000000000000000 ) ) ;
#14754=EDGE_LOOP ( 'NONE', ( #13653, #7872, #16416, #21069 ) ) ;
#14824=DIRECTION ( 'NONE',  ( -0.9997651245102160411, -0.02167246670483410909, 0.000000000000000000 ) ) ;
#14868=VECTOR ( 'NONE', #19065, 1000.000000000000114 ) ;
#14932=DIRECTION ( 'NONE',  ( 2.982858504577319616E-17, -2.441916418604790135E-15, -1.000000000000000000 ) ) ;
#14938=ORIENTED_EDGE ( 'NONE', *, *, #3909, .F. ) ;
#14940=AXIS2_PLACEMENT_3D ( 'NONE', #3162, #17659, #8625 ) ;
#14960=LINE ( 'NONE', #20422, #19256 ) ;
#14964=ORIENTED_EDGE ( 'NONE', *, *, #11862, .F. ) ;
#14993=CYLINDRICAL_SURFACE ( 'NONE', #6053, 2.499999999999999112 ) ;
#15015=LINE ( 'NONE', #20830, #14868 ) ;
#15033=EDGE_CURVE ( 'NONE', #17965, #4802, #4464, .T. ) ;
#15050=DIRECTION ( 'NONE',  ( -2.982858504577314686E-17, 2.441916418604790135E-15, 1.000000000000000000 ) ) ;
#15169=FACE_OUTER_BOUND ( 'NONE', #17102, .T. ) ;
#15238=DIRECTION ( 'NONE',  ( 2.982858504577314686E-17, -2.441916418604790135E-15, -1.000000000000000000 ) ) ;
#15276=ORIENTED_EDGE ( 'NONE', *, *, #16872, .T. ) ;
#15373=CARTESIAN_POINT ( 'NONE',  ( -21.66385406723090057, 11.15564796089419985, 5.000000000000000000 ) ) ;
#15380=CARTESIAN_POINT ( 'NONE',  ( -32.64674982798959491, 7.329300507370480666, 3.750000000000000000 ) ) ;
#15397=FACE_OUTER_BOUND ( 'NONE', #3411, .T. ) ;
#15436=VECTOR ( 'NONE', #20963, 1000.000000000000000 ) ;
#15481=DIRECTION ( 'NONE',  ( -0.9080618652418041004, 0.4188360644614733674, -1.040834085574019418E-15 ) ) ;
#15585=AXIS2_PLACEMENT_3D ( 'NONE', #47, #21549, #7322 ) ;
#15600=EDGE_CURVE ( 'NONE', #18635, #9514, #16578, .T. ) ;
#15683=ORIENTED_EDGE ( 'NONE', *, *, #15951, .F. ) ;
#15741=ADVANCED_FACE ( 'NONE', ( #11276 ), #18508, .F. ) ;
#15806=DIRECTION ( 'NONE',  ( 0.02167246311338769799, -0.9997651245880698756, 2.441989331389200018E-15 ) ) ;
#15889=FACE_OUTER_BOUND ( 'NONE', #17101, .T. ) ;
#15951=EDGE_CURVE ( 'NONE', #20315, #8432, #19752, .T. ) ;
#16013=ORIENTED_EDGE ( 'NONE', *, *, #21053, .T. ) ;
#16016=ADVANCED_FACE ( 'NONE', ( #251 ), #21766, .T. ) ;
#16044=CARTESIAN_POINT ( 'NONE',  ( -16.50058068176714343, 23.02794805996801841, 5.000000000000000000 ) ) ;
#16225=AXIS2_PLACEMENT_3D ( 'NONE', #21894, #39, #12663 ) ;
#16265=CARTESIAN_POINT ( 'NONE',  ( -19.49999999982360066, -0.1021026942259639914, 2.500000000000000000 ) ) ;
#16293=CARTESIAN_POINT ( 'NONE',  ( -25.44812980900369936, 25.46511081327010118, 3.749999999999940048 ) ) ;
#16416=ORIENTED_EDGE ( 'NONE', *, *, #6081, .T. ) ;
#16463=VERTEX_POINT ( 'NONE', #16044 ) ;
#16545=AXIS2_PLACEMENT_3D ( 'NONE', #14397, #3357, #7060 ) ;
#16578=LINE ( 'NONE', #9472, #11091 ) ;
#16584=AXIS2_PLACEMENT_3D ( 'NONE', #1731, #10558, #19564 ) ;
#16611=DIRECTION ( 'NONE',  ( -7.283891156702289181E-32, 2.441916418604790135E-15, 1.000000000000000000 ) ) ;
#16625=VECTOR ( 'NONE', #7225, 1000.000000000000114 ) ;
#16809=DIRECTION ( 'NONE',  ( 0.000000000000000000, -2.442072289818050260E-15, -1.000000000000000000 ) ) ;
#16827=EDGE_LOOP ( 'NONE', ( #11633, #14964, #21429, #6965, #21140, #7297, #5573, #1642, #1661, #4012, #438 ) ) ;
#16836=LINE ( 'NONE', #7814, #13800 ) ;
#16871=EDGE_CURVE ( 'NONE', #4802, #17965, #20589, .T. ) ;
#16872=EDGE_CURVE ( 'NONE', #7533, #9579, #3534, .T. ) ;
#16892=DIRECTION ( 'NONE',  ( -2.982858504577314686E-17, 2.441916418604790135E-15, 1.000000000000000000 ) ) ;
#16911=ADVANCED_FACE ( 'NONE', ( #17803 ), #12582, .T. ) ;
#16921=ORIENTED_EDGE ( 'NONE', *, *, #1441, .T. ) ;
#16964=CARTESIAN_POINT ( 'NONE',  ( 34.24699604337060066, 12.59578995394270073, 5.000000000000000000 ) ) ;
#16982=MANIFOLD_SOLID_BREP ( 'Imported1', #12484 ) ;
#17035=CIRCLE ( 'NONE', #8329, 49.22658835543909817 ) ;
#17090=DIRECTION ( 'NONE',  ( -2.982858504577319616E-17, 2.441916418604790135E-15, 1.000000000000000000 ) ) ;
#17092=DIRECTION ( 'NONE',  ( 0.005225493764075828107, -0.9999863470142589250, 2.602085213965210642E-15 ) ) ;
#17101=EDGE_LOOP ( 'NONE', ( #5534, #4459, #2253, #11462 ) ) ;
#17102=EDGE_LOOP ( 'NONE', ( #12012, #15683, #13525, #13436 ) ) ;
#17143=EDGE_CURVE ( 'NONE', #23068, #8432, #18237, .T. ) ;
#17197=DIRECTION ( 'NONE',  ( -2.982858504577314686E-17, 2.441916418604790135E-15, 1.000000000000000000 ) ) ;
#17254=EDGE_CURVE ( 'NONE', #18635, #20315, #11157, .T. ) ;
#17351=AXIS2_PLACEMENT_3D ( 'NONE', #12195, #3154, #6838 ) ;
#17354=EDGE_CURVE ( 'NONE', #22503, #21418, #105, .T. ) ;
#17370=CYLINDRICAL_SURFACE ( 'NONE', #10361, 3.500000000000000444 ) ;
#17574=VECTOR ( 'NONE', #21253, 1000.000000000000000 ) ;
#17587=ADVANCED_BREP_SHAPE_REPRESENTATION ( '', ( #16982, #12739 ), #14249 ) ;
#17604=LINE ( 'NONE', #12031, #23397 ) ;
#17630=CARTESIAN_POINT ( 'NONE',  ( -30.15694676875160241, 9.287188980624559775, 2.500000000000000000 ) ) ;
#17659=DIRECTION ( 'NONE',  ( -2.982858504577319616E-17, 2.441916418604790135E-15, 1.000000000000000000 ) ) ;
#17675=ORIENTED_EDGE ( 'NONE', *, *, #6445, .F. ) ;
#17742=AXIS2_PLACEMENT_3D ( 'NONE', #16265, #9550, #1888 ) ;
#17753=DIRECTION ( 'NONE',  ( -2.982858504577319616E-17, 2.441916418604790135E-15, 1.000000000000000000 ) ) ;
#17765=CIRCLE ( 'NONE', #20774, 6.000000000001507239 ) ;
#17766=FACE_OUTER_BOUND ( 'NONE', #8751, .T. ) ;
#17797=CARTESIAN_POINT ( 'NONE',  ( -25.49859074735509878, -0.2321374729090499855, 3.750000000000000000 ) ) ;
#17803=FACE_OUTER_BOUND ( 'NONE', #18660, .T. ) ;
#17834=EDGE_CURVE ( 'NONE', #18753, #7665, #21380, .T. ) ;
#17933=VECTOR ( 'NONE', #9096, 1000.000000000000114 ) ;
#17965=VERTEX_POINT ( 'NONE', #3418 ) ;
#17985=PLANE ( 'NONE',  #23360 ) ;
#18016=CARTESIAN_POINT ( 'NONE',  ( -32.64674982798959491, 7.329300507370470008, 2.500000000000000000 ) ) ;
#18148=LINE ( 'NONE', #12691, #16625 ) ;
#18237=LINE ( 'NONE', #10658, #6198 ) ;
#18264=ADVANCED_FACE ( 'NONE', ( #15397 ), #10081, .T. ) ;
#18280=ORIENTED_EDGE ( 'NONE', *, *, #21053, .F. ) ;
#18285=CARTESIAN_POINT ( 'NONE',  ( -19.49999999982360066, -0.1021026942259579962, 5.000000000000000000 ) ) ;
#18407=EDGE_CURVE ( 'NONE', #4802, #7660, #16836, .T. ) ;
#18414=DIRECTION ( 'NONE',  ( -0.9999863470142589250, -0.005225493764064552404, 0.000000000000000000 ) ) ;
#18456=AXIS2_PLACEMENT_3D ( 'NONE', #22041, #11275, #78 ) ;
#18495=VERTEX_POINT ( 'NONE', #21451 ) ;
#18508=CYLINDRICAL_SURFACE ( 'NONE', #9176, 49.22658835543909817 ) ;
#18575=DIRECTION ( 'NONE',  ( 2.982858504577240114E-17, -2.441916418604790135E-15, -1.000000000000000000 ) ) ;
#18624=DIRECTION ( 'NONE',  ( -0.9997651245102160411, -0.02167246670483410909, 0.000000000000000000 ) ) ;
#18635=VERTEX_POINT ( 'NONE', #20137 ) ;
#18644=EDGE_CURVE ( 'NONE', #18495, #18753, #1841, .T. ) ;
#18658=ORIENTED_EDGE ( 'NONE', *, *, #16871, .T. ) ;
#18660=EDGE_LOOP ( 'NONE', ( #2841, #20911, #20336, #4042 ) ) ;
#18725=AXIS2_PLACEMENT_3D ( 'NONE', #8555, #19232, #22780 ) ;
#18753=VERTEX_POINT ( 'NONE', #18016 ) ;
#18770=DIRECTION ( 'NONE',  ( -1.156142442796728099E-15, -6.608067939030890210E-32, 1.000000000000000000 ) ) ;
#18827=ADVANCED_FACE ( 'NONE', ( #18843, #13245, #13596 ), #22603, .T. ) ;
#18843=FACE_BOUND ( 'NONE', #21011, .T. ) ;
#18972=DIRECTION ( 'NONE',  ( -0.9997651245880592175, -0.02167246311387460711, 0.000000000000000000 ) ) ;
#19042=CARTESIAN_POINT ( 'NONE',  ( -19.49999999982360066, -0.1021026942259609938, 3.750000000000000000 ) ) ;
#19065=DIRECTION ( 'NONE',  ( -0.02167246311338769799, 0.9997651245880698756, -2.441989331389200018E-15 ) ) ;
#19157=FACE_OUTER_BOUND ( 'NONE', #10140, .T. ) ;
#19159=EDGE_CURVE ( 'NONE', #21418, #6041, #7415, .T. ) ;
#19183=EDGE_LOOP ( 'NONE', ( #2163, #17675, #14093, #14938, #5729, #21008, #9158, #1792, #5353, #22199, #4132 ) ) ;
#19232=DIRECTION ( 'NONE',  ( -2.982858504577314686E-17, 2.441916418604790135E-15, 1.000000000000000000 ) ) ;
#19236=EDGE_LOOP ( 'NONE', ( #22317, #3391, #6060, #20893 ) ) ;
#19256=VECTOR ( 'NONE', #17090, 1000.000000000000000 ) ;
#19312=ORIENTED_EDGE ( 'NONE', *, *, #5454, .F. ) ;
#19335=ORIENTED_EDGE ( 'NONE', *, *, #22048, .F. ) ;
#19336=EDGE_LOOP ( 'NONE', ( #11588, #167 ) ) ;
#19461=ORIENTED_EDGE ( 'NONE', *, *, #21558, .T. ) ;
#19564=DIRECTION ( 'NONE',  ( -0.9997651245102161521, -0.02167246670483386276, 0.000000000000000000 ) ) ;
#19588=CARTESIAN_POINT ( 'NONE',  ( -23.49893655333865894, 22.87624079303418156, 2.499999999999950262 ) ) ;
#19590=DIRECTION ( 'NONE',  ( -2.982858504577319616E-17, 2.441916418604790135E-15, 1.000000000000000000 ) ) ;
#19620=DIRECTION ( 'NONE',  ( 2.982858504577314686E-17, -2.441916418604790135E-15, -1.000000000000000000 ) ) ;
#19635=ORIENTED_EDGE ( 'NONE', *, *, #11271, .F. ) ;
#19660=ORIENTED_EDGE ( 'NONE', *, *, #17354, .T. ) ;
#19752=LINE ( 'NONE', #16293, #11860 ) ;
#19878=CARTESIAN_POINT ( 'NONE',  ( -32.64674982798959491, 7.329300507370480666, 3.750000000000000000 ) ) ;
#19898=EDGE_CURVE ( 'NONE', #7665, #7533, #20992, .T. ) ;
#19984=CARTESIAN_POINT ( 'NONE',  ( -27.39120887301850260, 6.327965799971409844, 2.500000000000000000 ) ) ;
#19986=DIRECTION ( 'NONE',  ( -0.9080618652418041004, 0.4188360644614733674, -1.040834085574019418E-15 ) ) ;
#19990=VERTEX_POINT ( 'NONE', #2476 ) ;
#20081=AXIS2_PLACEMENT_3D ( 'NONE', #20544, #20428, #4158 ) ;
#20137=CARTESIAN_POINT ( 'NONE',  ( -14.10640258711669937, 21.82649101058139962, 2.499999999999950262 ) ) ;
#20277=EDGE_LOOP ( 'NONE', ( #13837, #14566, #4533, #21574 ) ) ;
#20315=VERTEX_POINT ( 'NONE', #643 ) ;
#20336=ORIENTED_EDGE ( 'NONE', *, *, #17254, .T. ) ;
#20350=CARTESIAN_POINT ( 'NONE',  ( -29.01753512594849838, 6.974156885510950588, 5.000000000000000000 ) ) ;
#20422=CARTESIAN_POINT ( 'NONE',  ( -29.01753512594849838, 6.974156885510950588, 3.750000000000000000 ) ) ;
#20428=DIRECTION ( 'NONE',  ( 2.982858504577314686E-17, -2.441916418604790135E-15, -1.000000000000000000 ) ) ;
#20452=VERTEX_POINT ( 'NONE', #2319 ) ;
#20457=ADVANCED_FACE ( 'NONE', ( #13249 ), #20486, .T. ) ;
#20463=CARTESIAN_POINT ( 'NONE',  ( -25.44812980900369936, 25.46511081327010118, 2.499999999999940048 ) ) ;
#20484=ORIENTED_EDGE ( 'NONE', *, *, #6445, .T. ) ;
#20486=CYLINDRICAL_SURFACE ( 'NONE', #20593, 1.000000000000000000 ) ;
#20544=CARTESIAN_POINT ( 'NONE',  ( -19.49999999982360066, -0.1021026942259579962, 5.000000000000000000 ) ) ;
#20581=VECTOR ( 'NONE', #9365, 1000.000000000000000 ) ;
#20589=CIRCLE ( 'NONE', #18725, 2.499999999999999112 ) ;
#20593=AXIS2_PLACEMENT_3D ( 'NONE', #4221, #11496, #22507 ) ;
#20641=ORIENTED_EDGE ( 'NONE', *, *, #15033, .T. ) ;
#20740=CARTESIAN_POINT ( 'NONE',  ( -19.49999999982360066, -0.1021026942259609938, 3.750000000000000000 ) ) ;
#20774=AXIS2_PLACEMENT_3D ( 'NONE', #13529, #6655, #3073 ) ;
#20830=CARTESIAN_POINT ( 'NONE',  ( -25.64161990512560152, 6.365892616704879714, 5.000000000000000000 ) ) ;
#20853=EDGE_CURVE ( 'NONE', #20315, #10599, #5975, .T. ) ;
#20893=ORIENTED_EDGE ( 'NONE', *, *, #5454, .T. ) ;
#20911=ORIENTED_EDGE ( 'NONE', *, *, #15600, .F. ) ;
#20963=DIRECTION ( 'NONE',  ( -2.982858504577319616E-17, 2.441916418604790135E-15, 1.000000000000000000 ) ) ;
#20982=DIRECTION ( 'NONE',  ( -2.982858504577314686E-17, 2.441916418604790135E-15, 1.000000000000000000 ) ) ;
#20992=LINE ( 'NONE', #4603, #21687 ) ;
#21008=ORIENTED_EDGE ( 'NONE', *, *, #22323, .F. ) ;
#21011=EDGE_LOOP ( 'NONE', ( #16921, #16013 ) ) ;
#21053=EDGE_CURVE ( 'NONE', #16463, #1745, #12657, .T. ) ;
#21069=ORIENTED_EDGE ( 'NONE', *, *, #15600, .T. ) ;
#21140=ORIENTED_EDGE ( 'NONE', *, *, #16872, .F. ) ;
#21215=CYLINDRICAL_SURFACE ( 'NONE', #16584, 3.500000000000000444 ) ;
#21253=DIRECTION ( 'NONE',  ( -2.982858504577314686E-17, 2.441916418604790135E-15, 1.000000000000000000 ) ) ;
#21364=CARTESIAN_POINT ( 'NONE',  ( -19.99995718853209681, 22.95166395734839782, 3.749999999999949818 ) ) ;
#21380=CIRCLE ( 'NONE', #21768, 1.000000000000000000 ) ;
#21411=CARTESIAN_POINT ( 'NONE',  ( -14.10640258711669937, 21.82649101058139962, 5.000000000000000000 ) ) ;
#21418=VERTEX_POINT ( 'NONE', #22206 ) ;
#21429=ORIENTED_EDGE ( 'NONE', *, *, #14709, .F. ) ;
#21445=FACE_OUTER_BOUND ( 'NONE', #22387, .T. ) ;
#21451=CARTESIAN_POINT ( 'NONE',  ( -32.65691263631629226, 9.274125246214069307, 2.500000000000000000 ) ) ;
#21521=EDGE_LOOP ( 'NONE', ( #8906, #2962 ) ) ;
#21549=DIRECTION ( 'NONE',  ( 2.982858504577324546E-17, -2.441916418604790135E-15, -1.000000000000000000 ) ) ;
#21558=EDGE_CURVE ( 'NONE', #8426, #22503, #14269, .T. ) ;
#21574=ORIENTED_EDGE ( 'NONE', *, *, #11271, .T. ) ;
#21642=CARTESIAN_POINT ( 'NONE',  ( -31.64153798721130428, 6.334539654120280083, 5.000000000000000000 ) ) ;
#21687=VECTOR ( 'NONE', #22636, 1000.000000000000114 ) ;
#21764=DIRECTION ( 'NONE',  ( -0.9997651245102161521, -0.02167246670483388357, 0.000000000000000000 ) ) ;
#21766=CYLINDRICAL_SURFACE ( 'NONE', #6536, 2.500000000028978597 ) ;
#21768=AXIS2_PLACEMENT_3D ( 'NONE', #6175, #13428, #22779 ) ;
#21835=ADVANCED_FACE ( 'NONE', ( #21445 ), #2929, .F. ) ;
#21871=AXIS2_PLACEMENT_3D ( 'NONE', #17630, #2786, #15481 ) ;
#21893=EDGE_CURVE ( 'NONE', #17965, #3931, #22746, .T. ) ;
#21894=CARTESIAN_POINT ( 'NONE',  ( -19.99975861755289941, 22.95209442650110176, 2.499999999999950262 ) ) ;
#21920=ORIENTED_EDGE ( 'NONE', *, *, #2082, .T. ) ;
#22041=CARTESIAN_POINT ( 'NONE',  ( -27.39120887301850260, 6.327965799971420502, 5.000000000000000000 ) ) ;
#22048=EDGE_CURVE ( 'NONE', #18753, #5830, #293, .T. ) ;
#22066=DIRECTION ( 'NONE',  ( 2.982858504577319616E-17, -2.441916418604790135E-15, -1.000000000000000000 ) ) ;
#22092=CARTESIAN_POINT ( 'NONE',  ( -23.49893655333865894, 22.87624079303418156, 5.000000000000000000 ) ) ;
#22095=CIRCLE ( 'NONE', #6954, 1.000000000000000000 ) ;
#22132=DIRECTION ( 'NONE',  ( -2.982858504577314686E-17, 2.441916418604790135E-15, 1.000000000000000000 ) ) ;
#22147=AXIS2_PLACEMENT_3D ( 'NONE', #16964, #6161, #686 ) ;
#22165=DIRECTION ( 'NONE',  ( -2.982858504577319616E-17, 2.441916418604790135E-15, 1.000000000000000000 ) ) ;
#22175=CARTESIAN_POINT ( 'NONE',  ( -25.44852691694969948, 25.46424985927700035, 3.749999999999940048 ) ) ;
#22182=CARTESIAN_POINT ( 'NONE',  ( -31.64676348097539815, 7.334526001134540785, 5.000000000000000000 ) ) ;
#22199=ORIENTED_EDGE ( 'NONE', *, *, #17354, .F. ) ;
#22206=CARTESIAN_POINT ( 'NONE',  ( -29.94163891957289891, 6.343422587376370103, 5.000000000000000000 ) ) ;
#22309=VECTOR ( 'NONE', #14932, 1000.000000000000000 ) ;
#22317=ORIENTED_EDGE ( 'NONE', *, *, #22323, .T. ) ;
#22323=EDGE_CURVE ( 'NONE', #20452, #23068, #10158, .T. ) ;
#22387=EDGE_LOOP ( 'NONE', ( #19461, #6055, #13258, #7101 ) ) ;
#22472=CARTESIAN_POINT ( 'NONE',  ( 34.24699604337060066, 12.59578995394270073, 2.499999999999970246 ) ) ;
#22503=VERTEX_POINT ( 'NONE', #20350 ) ;
#22507=DIRECTION ( 'NONE',  ( 0.005225493764075828107, -0.9999863470142589250, 2.602085213965210642E-15 ) ) ;
#22603=PLANE ( 'NONE',  #10745 ) ;
#22636=DIRECTION ( 'NONE',  ( 0.9999863470142587030, 0.005225493764090578461, 1.706795877867719251E-17 ) ) ;
#22746=LINE ( 'NONE', #4715, #10532 ) ;
#22779=DIRECTION ( 'NONE',  ( -0.9999863470142589250, -0.005225493764064552404, 0.000000000000000000 ) ) ;
#22780=DIRECTION ( 'NONE',  ( -0.9997651245102160411, -0.02167246670483411256, 0.000000000000000000 ) ) ;
#23068=VERTEX_POINT ( 'NONE', #321 ) ;
#23092=DIRECTION ( 'NONE',  ( -2.982858504577314686E-17, 2.441916418604790135E-15, 1.000000000000000000 ) ) ;
#23153=CARTESIAN_POINT ( 'NONE',  ( -19.99975861755289941, 22.95209442650110176, 3.749999999999949818 ) ) ;
#23360=AXIS2_PLACEMENT_3D ( 'NONE', #19878, #3601, #10870 ) ;
#23397=VECTOR ( 'NONE', #15806, 1000.000000000000114 ) ;
#23435=( NAMED_UNIT ( * ) SI_UNIT ( $, .STERADIAN. ) SOLID_ANGLE_UNIT ( ) );
#23529=COLOUR_RGB('Sky Blue', 0.31764706, 0.68627451, 0.89019608);
#23530=FILL_AREA_STYLE_COLOUR('',#23529);
#23531=FILL_AREA_STYLE('',(#23530));
#23532=SURFACE_STYLE_FILL_AREA(#23531);
#23533=SURFACE_SIDE_STYLE('',(#23532));
#23534=SURFACE_STYLE_USAGE(.BOTH.,#23533);
#23535=PRESENTATION_STYLE_ASSIGNMENT((#23534));
#23613=STYLED_ITEM('',(#23535),#16982);
#23614=MECHANICAL_DESIGN_GEOMETRIC_PRESENTATION_REPRESENTATION('',(#23613),#14249);
ENDSEC;
END-ISO-10303-21;
